ISO-10303-21;
HEADER;
/* Generated by software containing ST-Developer
 * from STEP Tools, Inc. (www.steptools.com) 
 */

FILE_DESCRIPTION(
/* description */ ('Belt conveyor head drive unit'),
/* implementation_level */ '2;1');

FILE_NAME(
/* name */ 'Cap Screw - M4x16.step',
/* time_stamp */ '2026-10-28T03:26:19-07:00',
/* author */ (''),
/* organization */ (''),
/* preprocessor_version */ 'ST-DEVELOPER v20.2',
/* originating_system */ 'Autodesk Translation Framework v15.17.0.0',
/* authorisation */ '');

FILE_SCHEMA (('AUTOMOTIVE_DESIGN { 1 0 10303 214 3 1 1 }'));
ENDSEC;

DATA;
#10=MECHANICAL_DESIGN_GEOMETRIC_PRESENTATION_REPRESENTATION('',(#930),#27069);
#15=ORIENTED_CLOSED_SHELL('',*,#13800,.F.);
#20=BREP_WITH_VOIDS('Body1',#13799,(#15));
#699=CONICAL_SURFACE('',#16281,0.325,0.785398163397448);
#700=CONICAL_SURFACE('',#16285,0.335,0.785398163397448);
#701=CONICAL_SURFACE('',#16289,0.21,0.463647609000806);
#702=CONICAL_SURFACE('',#16293,0.18,0.785398163397448);
#776=SHAPE_REPRESENTATION_RELATIONSHIP('SRR','None',#27425,#845);
#845=ADVANCED_BREP_SHAPE_REPRESENTATION('',(#20),#27067);
#930=STYLED_ITEM('',(#27804),#20);
#1275=FACE_BOUND('',#3472,.T.);
#1613=PLANE('',#16279);
#1614=PLANE('',#16287);
#1615=PLANE('',#16295);
#1616=PLANE('',#16296);
#1617=PLANE('',#16297);
#1618=PLANE('',#16298);
#1619=PLANE('',#16299);
#1620=PLANE('',#16300);
#1621=PLANE('',#16301);
#1622=PLANE('',#16302);
#1623=PLANE('',#16303);
#2404=FACE_OUTER_BOUND('',#3467,.T.);
#2405=FACE_OUTER_BOUND('',#3468,.T.);
#2406=FACE_OUTER_BOUND('',#3469,.T.);
#2407=FACE_OUTER_BOUND('',#3470,.T.);
#2408=FACE_OUTER_BOUND('',#3471,.T.);
#2409=FACE_OUTER_BOUND('',#3473,.T.);
#2410=FACE_OUTER_BOUND('',#3474,.T.);
#2411=FACE_OUTER_BOUND('',#3475,.T.);
#2412=FACE_OUTER_BOUND('',#3476,.T.);
#2413=FACE_OUTER_BOUND('',#3477,.T.);
#2414=FACE_OUTER_BOUND('',#3478,.T.);
#2415=FACE_OUTER_BOUND('',#3479,.T.);
#2416=FACE_OUTER_BOUND('',#3480,.T.);
#2417=FACE_OUTER_BOUND('',#3481,.T.);
#2418=FACE_OUTER_BOUND('',#3482,.T.);
#2419=FACE_OUTER_BOUND('',#3483,.T.);
#2420=FACE_OUTER_BOUND('',#3484,.T.);
#3467=EDGE_LOOP('',(#12418));
#3468=EDGE_LOOP('',(#12419,#12420,#12421,#12422));
#3469=EDGE_LOOP('',(#12423,#12424,#12425,#12426));
#3470=EDGE_LOOP('',(#12427,#12428,#12429,#12430));
#3471=EDGE_LOOP('',(#12431));
#3472=EDGE_LOOP('',(#12432));
#3473=EDGE_LOOP('',(#12433,#12434,#12435,#12436));
#3474=EDGE_LOOP('',(#12437,#12438,#12439,#12440));
#3475=EDGE_LOOP('',(#12441,#12442,#12443,#12444));
#3476=EDGE_LOOP('',(#12445));
#3477=EDGE_LOOP('',(#12446,#12447,#12448,#12449));
#3478=EDGE_LOOP('',(#12450,#12451,#12452,#12453));
#3479=EDGE_LOOP('',(#12454,#12455,#12456,#12457));
#3480=EDGE_LOOP('',(#12458,#12459,#12460,#12461));
#3481=EDGE_LOOP('',(#12462,#12463,#12464,#12465));
#3482=EDGE_LOOP('',(#12466,#12467,#12468,#12469));
#3483=EDGE_LOOP('',(#12470,#12471,#12472,#12473,#12474,#12475));
#3484=EDGE_LOOP('',(#12476,#12477,#12478,#12479,#12480,#12481));
#4245=LINE('',#26686,#5037);
#4246=LINE('',#26690,#5038);
#4247=LINE('',#26694,#5039);
#4248=LINE('',#26701,#5040);
#4249=LINE('',#26705,#5041);
#4250=LINE('',#26709,#5042);
#4251=LINE('',#26714,#5043);
#4252=LINE('',#26716,#5044);
#4253=LINE('',#26718,#5045);
#4254=LINE('',#26719,#5046);
#4255=LINE('',#26722,#5047);
#4256=LINE('',#26724,#5048);
#4257=LINE('',#26725,#5049);
#4258=LINE('',#26728,#5050);
#4259=LINE('',#26730,#5051);
#4260=LINE('',#26731,#5052);
#4261=LINE('',#26734,#5053);
#4262=LINE('',#26736,#5054);
#4263=LINE('',#26737,#5055);
#4264=LINE('',#26740,#5056);
#4265=LINE('',#26742,#5057);
#4266=LINE('',#26743,#5058);
#4267=LINE('',#26745,#5059);
#4268=LINE('',#26746,#5060);
#5037=VECTOR('',#20623,0.325);
#5038=VECTOR('',#20628,0.35);
#5039=VECTOR('',#20633,0.335);
#5040=VECTOR('',#20642,0.21);
#5041=VECTOR('',#20647,0.2);
#5042=VECTOR('',#20652,0.18);
#5043=VECTOR('',#20657,1.);
#5044=VECTOR('',#20658,1.);
#5045=VECTOR('',#20659,1.);
#5046=VECTOR('',#20660,1.);
#5047=VECTOR('',#20663,1.);
#5048=VECTOR('',#20664,1.);
#5049=VECTOR('',#20665,1.);
#5050=VECTOR('',#20668,1.);
#5051=VECTOR('',#20669,1.);
#5052=VECTOR('',#20670,1.);
#5053=VECTOR('',#20673,1.);
#5054=VECTOR('',#20674,1.);
#5055=VECTOR('',#20675,1.);
#5056=VECTOR('',#20678,1.);
#5057=VECTOR('',#20679,1.);
#5058=VECTOR('',#20680,1.);
#5059=VECTOR('',#20683,1.);
#5060=VECTOR('',#20684,1.);
#5941=CIRCLE('',#16280,0.3);
#5942=CIRCLE('',#16282,0.35);
#5943=CIRCLE('',#16284,0.35);
#5944=CIRCLE('',#16286,0.32);
#5945=CIRCLE('',#16288,0.22);
#5946=CIRCLE('',#16290,0.1954);
#5947=CIRCLE('',#16292,0.1954);
#5948=CIRCLE('',#16294,0.16);
#7135=VERTEX_POINT('',#26681);
#7136=VERTEX_POINT('',#26684);
#7137=VERTEX_POINT('',#26688);
#7138=VERTEX_POINT('',#26692);
#7139=VERTEX_POINT('',#26696);
#7140=VERTEX_POINT('',#26699);
#7141=VERTEX_POINT('',#26703);
#7142=VERTEX_POINT('',#26707);
#7143=VERTEX_POINT('',#26712);
#7144=VERTEX_POINT('',#26713);
#7145=VERTEX_POINT('',#26715);
#7146=VERTEX_POINT('',#26717);
#7147=VERTEX_POINT('',#26721);
#7148=VERTEX_POINT('',#26723);
#7149=VERTEX_POINT('',#26727);
#7150=VERTEX_POINT('',#26729);
#7151=VERTEX_POINT('',#26733);
#7152=VERTEX_POINT('',#26735);
#7153=VERTEX_POINT('',#26739);
#7154=VERTEX_POINT('',#26741);
#8901=EDGE_CURVE('',#7135,#7135,#5941,.T.);
#8902=EDGE_CURVE('',#7136,#7136,#5942,.T.);
#8903=EDGE_CURVE('',#7136,#7135,#4245,.T.);
#8904=EDGE_CURVE('',#7137,#7137,#5943,.T.);
#8905=EDGE_CURVE('',#7137,#7136,#4246,.T.);
#8906=EDGE_CURVE('',#7138,#7138,#5944,.T.);
#8907=EDGE_CURVE('',#7138,#7137,#4247,.T.);
#8908=EDGE_CURVE('',#7139,#7139,#5945,.T.);
#8909=EDGE_CURVE('',#7140,#7140,#5946,.F.);
#8910=EDGE_CURVE('',#7140,#7139,#4248,.T.);
#8911=EDGE_CURVE('',#7141,#7141,#5947,.F.);
#8912=EDGE_CURVE('',#7141,#7140,#4249,.T.);
#8913=EDGE_CURVE('',#7142,#7142,#5948,.T.);
#8914=EDGE_CURVE('',#7142,#7141,#4250,.T.);
#8915=EDGE_CURVE('',#7143,#7144,#4251,.T.);
#8916=EDGE_CURVE('',#7144,#7145,#4252,.T.);
#8917=EDGE_CURVE('',#7145,#7146,#4253,.T.);
#8918=EDGE_CURVE('',#7143,#7146,#4254,.T.);
#8919=EDGE_CURVE('',#7144,#7147,#4255,.T.);
#8920=EDGE_CURVE('',#7147,#7148,#4256,.T.);
#8921=EDGE_CURVE('',#7148,#7145,#4257,.T.);
#8922=EDGE_CURVE('',#7147,#7149,#4258,.T.);
#8923=EDGE_CURVE('',#7149,#7150,#4259,.T.);
#8924=EDGE_CURVE('',#7150,#7148,#4260,.T.);
#8925=EDGE_CURVE('',#7149,#7151,#4261,.T.);
#8926=EDGE_CURVE('',#7151,#7152,#4262,.T.);
#8927=EDGE_CURVE('',#7152,#7150,#4263,.T.);
#8928=EDGE_CURVE('',#7151,#7153,#4264,.T.);
#8929=EDGE_CURVE('',#7153,#7154,#4265,.T.);
#8930=EDGE_CURVE('',#7154,#7152,#4266,.T.);
#8931=EDGE_CURVE('',#7153,#7143,#4267,.T.);
#8932=EDGE_CURVE('',#7146,#7154,#4268,.T.);
#12418=ORIENTED_EDGE('',*,*,#8901,.F.);
#12419=ORIENTED_EDGE('',*,*,#8902,.F.);
#12420=ORIENTED_EDGE('',*,*,#8903,.T.);
#12421=ORIENTED_EDGE('',*,*,#8901,.T.);
#12422=ORIENTED_EDGE('',*,*,#8903,.F.);
#12423=ORIENTED_EDGE('',*,*,#8904,.F.);
#12424=ORIENTED_EDGE('',*,*,#8905,.T.);
#12425=ORIENTED_EDGE('',*,*,#8902,.T.);
#12426=ORIENTED_EDGE('',*,*,#8905,.F.);
#12427=ORIENTED_EDGE('',*,*,#8906,.F.);
#12428=ORIENTED_EDGE('',*,*,#8907,.T.);
#12429=ORIENTED_EDGE('',*,*,#8904,.T.);
#12430=ORIENTED_EDGE('',*,*,#8907,.F.);
#12431=ORIENTED_EDGE('',*,*,#8906,.T.);
#12432=ORIENTED_EDGE('',*,*,#8908,.F.);
#12433=ORIENTED_EDGE('',*,*,#8909,.F.);
#12434=ORIENTED_EDGE('',*,*,#8910,.T.);
#12435=ORIENTED_EDGE('',*,*,#8908,.T.);
#12436=ORIENTED_EDGE('',*,*,#8910,.F.);
#12437=ORIENTED_EDGE('',*,*,#8911,.F.);
#12438=ORIENTED_EDGE('',*,*,#8912,.T.);
#12439=ORIENTED_EDGE('',*,*,#8909,.T.);
#12440=ORIENTED_EDGE('',*,*,#8912,.F.);
#12441=ORIENTED_EDGE('',*,*,#8913,.F.);
#12442=ORIENTED_EDGE('',*,*,#8914,.T.);
#12443=ORIENTED_EDGE('',*,*,#8911,.T.);
#12444=ORIENTED_EDGE('',*,*,#8914,.F.);
#12445=ORIENTED_EDGE('',*,*,#8913,.T.);
#12446=ORIENTED_EDGE('',*,*,#8915,.T.);
#12447=ORIENTED_EDGE('',*,*,#8916,.T.);
#12448=ORIENTED_EDGE('',*,*,#8917,.T.);
#12449=ORIENTED_EDGE('',*,*,#8918,.F.);
#12450=ORIENTED_EDGE('',*,*,#8919,.T.);
#12451=ORIENTED_EDGE('',*,*,#8920,.T.);
#12452=ORIENTED_EDGE('',*,*,#8921,.T.);
#12453=ORIENTED_EDGE('',*,*,#8916,.F.);
#12454=ORIENTED_EDGE('',*,*,#8922,.T.);
#12455=ORIENTED_EDGE('',*,*,#8923,.T.);
#12456=ORIENTED_EDGE('',*,*,#8924,.T.);
#12457=ORIENTED_EDGE('',*,*,#8920,.F.);
#12458=ORIENTED_EDGE('',*,*,#8925,.T.);
#12459=ORIENTED_EDGE('',*,*,#8926,.T.);
#12460=ORIENTED_EDGE('',*,*,#8927,.T.);
#12461=ORIENTED_EDGE('',*,*,#8923,.F.);
#12462=ORIENTED_EDGE('',*,*,#8928,.T.);
#12463=ORIENTED_EDGE('',*,*,#8929,.T.);
#12464=ORIENTED_EDGE('',*,*,#8930,.T.);
#12465=ORIENTED_EDGE('',*,*,#8926,.F.);
#12466=ORIENTED_EDGE('',*,*,#8931,.T.);
#12467=ORIENTED_EDGE('',*,*,#8918,.T.);
#12468=ORIENTED_EDGE('',*,*,#8932,.T.);
#12469=ORIENTED_EDGE('',*,*,#8929,.F.);
#12470=ORIENTED_EDGE('',*,*,#8931,.F.);
#12471=ORIENTED_EDGE('',*,*,#8928,.F.);
#12472=ORIENTED_EDGE('',*,*,#8925,.F.);
#12473=ORIENTED_EDGE('',*,*,#8922,.F.);
#12474=ORIENTED_EDGE('',*,*,#8919,.F.);
#12475=ORIENTED_EDGE('',*,*,#8915,.F.);
#12476=ORIENTED_EDGE('',*,*,#8932,.F.);
#12477=ORIENTED_EDGE('',*,*,#8917,.F.);
#12478=ORIENTED_EDGE('',*,*,#8921,.F.);
#12479=ORIENTED_EDGE('',*,*,#8924,.F.);
#12480=ORIENTED_EDGE('',*,*,#8927,.F.);
#12481=ORIENTED_EDGE('',*,*,#8930,.F.);
#12909=CYLINDRICAL_SURFACE('',#16283,0.35);
#12910=CYLINDRICAL_SURFACE('',#16291,0.1954);
#13683=ADVANCED_FACE('',(#2404),#1613,.T.);
#13684=ADVANCED_FACE('',(#2405),#699,.T.);
#13685=ADVANCED_FACE('',(#2406),#12909,.T.);
#13686=ADVANCED_FACE('',(#2407),#700,.T.);
#13687=ADVANCED_FACE('',(#2408,#1275),#1614,.T.);
#13688=ADVANCED_FACE('',(#2409),#701,.T.);
#13689=ADVANCED_FACE('',(#2410),#12910,.T.);
#13690=ADVANCED_FACE('',(#2411),#702,.T.);
#13691=ADVANCED_FACE('',(#2412),#1615,.T.);
#13692=ADVANCED_FACE('',(#2413),#1616,.F.);
#13693=ADVANCED_FACE('',(#2414),#1617,.F.);
#13694=ADVANCED_FACE('',(#2415),#1618,.F.);
#13695=ADVANCED_FACE('',(#2416),#1619,.F.);
#13696=ADVANCED_FACE('',(#2417),#1620,.F.);
#13697=ADVANCED_FACE('',(#2418),#1621,.F.);
#13698=ADVANCED_FACE('',(#2419),#1622,.F.);
#13699=ADVANCED_FACE('',(#2420),#1623,.F.);
#13799=CLOSED_SHELL('',(#13683,#13684,#13685,#13686,#13687,#13688,#13689,
#13690,#13691));
#13800=CLOSED_SHELL('',(#13692,#13693,#13694,#13695,#13696,#13697,#13698,
#13699));
#16278=AXIS2_PLACEMENT_3D('',#26679,#20613,#20614);
#16279=AXIS2_PLACEMENT_3D('',#26680,#20615,#20616);
#16280=AXIS2_PLACEMENT_3D('',#26682,#20617,#20618);
#16281=AXIS2_PLACEMENT_3D('',#26683,#20619,#20620);
#16282=AXIS2_PLACEMENT_3D('',#26685,#20621,#20622);
#16283=AXIS2_PLACEMENT_3D('',#26687,#20624,#20625);
#16284=AXIS2_PLACEMENT_3D('',#26689,#20626,#20627);
#16285=AXIS2_PLACEMENT_3D('',#26691,#20629,#20630);
#16286=AXIS2_PLACEMENT_3D('',#26693,#20631,#20632);
#16287=AXIS2_PLACEMENT_3D('',#26695,#20634,#20635);
#16288=AXIS2_PLACEMENT_3D('',#26697,#20636,#20637);
#16289=AXIS2_PLACEMENT_3D('',#26698,#20638,#20639);
#16290=AXIS2_PLACEMENT_3D('',#26700,#20640,#20641);
#16291=AXIS2_PLACEMENT_3D('',#26702,#20643,#20644);
#16292=AXIS2_PLACEMENT_3D('',#26704,#20645,#20646);
#16293=AXIS2_PLACEMENT_3D('',#26706,#20648,#20649);
#16294=AXIS2_PLACEMENT_3D('',#26708,#20650,#20651);
#16295=AXIS2_PLACEMENT_3D('',#26710,#20653,#20654);
#16296=AXIS2_PLACEMENT_3D('',#26711,#20655,#20656);
#16297=AXIS2_PLACEMENT_3D('',#26720,#20661,#20662);
#16298=AXIS2_PLACEMENT_3D('',#26726,#20666,#20667);
#16299=AXIS2_PLACEMENT_3D('',#26732,#20671,#20672);
#16300=AXIS2_PLACEMENT_3D('',#26738,#20676,#20677);
#16301=AXIS2_PLACEMENT_3D('',#26744,#20681,#20682);
#16302=AXIS2_PLACEMENT_3D('',#26747,#20685,#20686);
#16303=AXIS2_PLACEMENT_3D('',#26748,#20687,#20688);
#20613=DIRECTION('axis',(0.,0.,1.));
#20614=DIRECTION('refdir',(1.,0.,0.));
#20615=DIRECTION('center_axis',(0.,1.,0.));
#20616=DIRECTION('ref_axis',(0.,0.,1.));
#20617=DIRECTION('center_axis',(0.,-1.,0.));
#20618=DIRECTION('ref_axis',(1.,0.,0.));
#20619=DIRECTION('center_axis',(0.,-1.,0.));
#20620=DIRECTION('ref_axis',(1.,0.,0.));
#20621=DIRECTION('center_axis',(0.,-1.,0.));
#20622=DIRECTION('ref_axis',(1.,0.,0.));
#20623=DIRECTION('',(0.707106781186547,0.707106781186548,8.65956056235493E-17));
#20624=DIRECTION('center_axis',(0.,-1.,0.));
#20625=DIRECTION('ref_axis',(1.,0.,0.));
#20626=DIRECTION('center_axis',(0.,-1.,0.));
#20627=DIRECTION('ref_axis',(1.,0.,0.));
#20628=DIRECTION('',(0.,1.,0.));
#20629=DIRECTION('center_axis',(0.,1.,0.));
#20630=DIRECTION('ref_axis',(1.,0.,0.));
#20631=DIRECTION('center_axis',(0.,-1.,0.));
#20632=DIRECTION('ref_axis',(1.,0.,0.));
#20633=DIRECTION('',(-0.707106781186547,0.707106781186548,-8.65956056235493E-17));
#20634=DIRECTION('center_axis',(0.,-1.,0.));
#20635=DIRECTION('ref_axis',(0.,0.,-1.));
#20636=DIRECTION('center_axis',(0.,-1.,0.));
#20637=DIRECTION('ref_axis',(1.,0.,0.));
#20638=DIRECTION('center_axis',(0.,1.,0.));
#20639=DIRECTION('ref_axis',(1.,0.,0.));
#20640=DIRECTION('center_axis',(0.,1.,0.));
#20641=DIRECTION('ref_axis',(1.,0.,0.));
#20642=DIRECTION('',(-0.447213595499958,0.894427190999916,-5.47678698264203E-17));
#20643=DIRECTION('center_axis',(0.,-1.,0.));
#20644=DIRECTION('ref_axis',(1.,0.,0.));
#20645=DIRECTION('center_axis',(0.,1.,0.));
#20646=DIRECTION('ref_axis',(1.,0.,0.));
#20647=DIRECTION('',(0.,1.,0.));
#20648=DIRECTION('center_axis',(0.,1.,0.));
#20649=DIRECTION('ref_axis',(1.,0.,0.));
#20650=DIRECTION('center_axis',(0.,-1.,0.));
#20651=DIRECTION('ref_axis',(1.,0.,0.));
#20652=DIRECTION('',(-0.707106781186547,0.707106781186548,-8.65956056235493E-17));
#20653=DIRECTION('center_axis',(0.,-1.,0.));
#20654=DIRECTION('ref_axis',(0.,0.,-1.));
#20655=DIRECTION('center_axis',(0.866025403784439,0.,-0.5));
#20656=DIRECTION('ref_axis',(0.5,0.,0.866025403784439));
#20657=DIRECTION('',(-0.5,0.,-0.866025403784439));
#20658=DIRECTION('',(0.,-1.,0.));
#20659=DIRECTION('',(0.5,0.,0.866025403784439));
#20660=DIRECTION('',(0.,-1.,0.));
#20661=DIRECTION('center_axis',(1.60246890531964E-16,0.,-1.));
#20662=DIRECTION('ref_axis',(1.,0.,1.60246890531964E-16));
#20663=DIRECTION('',(-1.,0.,-1.60246890531964E-16));
#20664=DIRECTION('',(0.,-1.,0.));
#20665=DIRECTION('',(1.,0.,1.60246890531964E-16));
#20666=DIRECTION('center_axis',(-0.866025403784439,0.,-0.5));
#20667=DIRECTION('ref_axis',(0.5,0.,-0.866025403784439));
#20668=DIRECTION('',(-0.5,0.,0.866025403784439));
#20669=DIRECTION('',(0.,-1.,0.));
#20670=DIRECTION('',(0.5,0.,-0.866025403784439));
#20671=DIRECTION('center_axis',(-0.866025403784439,0.,0.5));
#20672=DIRECTION('ref_axis',(-0.5,0.,-0.866025403784439));
#20673=DIRECTION('',(0.5,0.,0.866025403784439));
#20674=DIRECTION('',(0.,-1.,0.));
#20675=DIRECTION('',(-0.5,0.,-0.866025403784439));
#20676=DIRECTION('center_axis',(-1.60246890531964E-16,0.,1.));
#20677=DIRECTION('ref_axis',(-1.,0.,-1.60246890531964E-16));
#20678=DIRECTION('',(1.,0.,1.60246890531964E-16));
#20679=DIRECTION('',(0.,-1.,0.));
#20680=DIRECTION('',(-1.,0.,-1.60246890531964E-16));
#20681=DIRECTION('center_axis',(0.866025403784439,0.,0.5));
#20682=DIRECTION('ref_axis',(-0.5,0.,0.866025403784439));
#20683=DIRECTION('',(0.5,0.,-0.866025403784439));
#20684=DIRECTION('',(-0.5,0.,0.866025403784439));
#20685=DIRECTION('center_axis',(0.,1.,0.));
#20686=DIRECTION('ref_axis',(1.,0.,0.));
#20687=DIRECTION('center_axis',(0.,-1.,0.));
#20688=DIRECTION('ref_axis',(0.,0.,-1.));
#26679=CARTESIAN_POINT('',(0.,0.,0.));
#26680=CARTESIAN_POINT('Origin',(0.3,0.4,0.));
#26681=CARTESIAN_POINT('',(-0.3,0.4,-3.67394039744206E-17));
#26682=CARTESIAN_POINT('Origin',(0.,0.4,0.));
#26683=CARTESIAN_POINT('Origin',(0.,0.375,0.));
#26684=CARTESIAN_POINT('',(-0.35,0.35,-4.28626379701573E-17));
#26685=CARTESIAN_POINT('Origin',(0.,0.35,0.));
#26686=CARTESIAN_POINT('',(-0.325,0.375,-3.9801020972289E-17));
#26687=CARTESIAN_POINT('Origin',(0.,0.19,0.));
#26688=CARTESIAN_POINT('',(-0.35,0.03,-4.28626379701574E-17));
#26689=CARTESIAN_POINT('Origin',(0.,0.03,0.));
#26690=CARTESIAN_POINT('',(-0.35,0.19,-4.28626379701574E-17));
#26691=CARTESIAN_POINT('Origin',(0.,0.0149999999999999,0.));
#26692=CARTESIAN_POINT('',(-0.32,-3.29597460435593E-17,-3.91886975727153E-17));
#26693=CARTESIAN_POINT('Origin',(0.,0.,0.));
#26694=CARTESIAN_POINT('',(-0.335,0.0149999999999999,-4.10256677714363E-17));
#26695=CARTESIAN_POINT('Origin',(0.22,0.,0.));
#26696=CARTESIAN_POINT('',(-0.22,-6.93889390390723E-18,-2.69422295812418E-17));
#26697=CARTESIAN_POINT('Origin',(0.,0.,0.));
#26698=CARTESIAN_POINT('Origin',(0.,-0.02,0.));
#26699=CARTESIAN_POINT('',(-0.1954,-0.0492,2.39295984553393E-17));
#26700=CARTESIAN_POINT('Origin',(0.,-0.0492,0.));
#26701=CARTESIAN_POINT('',(-0.21,-0.02,-2.57175827820944E-17));
#26702=CARTESIAN_POINT('Origin',(0.,-0.8,0.));
#26703=CARTESIAN_POINT('',(-0.1954,-1.5646,2.39295984553393E-17));
#26704=CARTESIAN_POINT('Origin',(0.,-1.5646,0.));
#26705=CARTESIAN_POINT('',(-0.1954,-0.8,-2.39295984553393E-17));
#26706=CARTESIAN_POINT('Origin',(0.,-1.58,0.));
#26707=CARTESIAN_POINT('',(-0.16,-1.6,-1.95943487863577E-17));
#26708=CARTESIAN_POINT('Origin',(0.,-1.6,0.));
#26709=CARTESIAN_POINT('',(-0.18,-1.58,-2.20436423846524E-17));
#26710=CARTESIAN_POINT('Origin',(0.,-1.6,0.));
#26711=CARTESIAN_POINT('Origin',(0.0866025403784439,-0.4,-0.15));
#26712=CARTESIAN_POINT('',(0.173205080756888,-0.4,0.));
#26713=CARTESIAN_POINT('',(0.0866025403784439,-0.4,-0.15));
#26714=CARTESIAN_POINT('',(0.173205080756888,-0.4,0.));
#26715=CARTESIAN_POINT('',(0.0866025403784439,-0.64,-0.15));
#26716=CARTESIAN_POINT('',(0.0866025403784439,-0.4,-0.15));
#26717=CARTESIAN_POINT('',(0.173205080756888,-0.64,0.));
#26718=CARTESIAN_POINT('',(0.173205080756888,-0.64,0.));
#26719=CARTESIAN_POINT('',(0.173205080756888,-0.4,0.));
#26720=CARTESIAN_POINT('Origin',(-0.0866025403784438,-0.4,-0.15));
#26721=CARTESIAN_POINT('',(-0.0866025403784438,-0.4,-0.15));
#26722=CARTESIAN_POINT('',(0.0866025403784439,-0.4,-0.15));
#26723=CARTESIAN_POINT('',(-0.0866025403784438,-0.64,-0.15));
#26724=CARTESIAN_POINT('',(-0.0866025403784438,-0.4,-0.15));
#26725=CARTESIAN_POINT('',(0.0866025403784439,-0.64,-0.15));
#26726=CARTESIAN_POINT('Origin',(-0.173205080756888,-0.4,-2.77555756156289E-17));
#26727=CARTESIAN_POINT('',(-0.173205080756888,-0.4,-2.12115047744981E-17));
#26728=CARTESIAN_POINT('',(-0.0866025403784438,-0.4,-0.15));
#26729=CARTESIAN_POINT('',(-0.173205080756888,-0.64,-2.77555756156289E-17));
#26730=CARTESIAN_POINT('',(-0.173205080756888,-0.4,-2.12115047744981E-17));
#26731=CARTESIAN_POINT('',(-0.0866025403784438,-0.64,-0.15));
#26732=CARTESIAN_POINT('Origin',(-0.0866025403784439,-0.4,0.15));
#26733=CARTESIAN_POINT('',(-0.0866025403784439,-0.4,0.15));
#26734=CARTESIAN_POINT('',(-0.173205080756888,-0.4,-2.12115047744981E-17));
#26735=CARTESIAN_POINT('',(-0.0866025403784439,-0.64,0.15));
#26736=CARTESIAN_POINT('',(-0.0866025403784439,-0.4,0.15));
#26737=CARTESIAN_POINT('',(-0.173205080756888,-0.64,-2.12115047744981E-17));
#26738=CARTESIAN_POINT('Origin',(0.0866025403784439,-0.4,0.15));
#26739=CARTESIAN_POINT('',(0.0866025403784439,-0.4,0.15));
#26740=CARTESIAN_POINT('',(-0.0866025403784439,-0.4,0.15));
#26741=CARTESIAN_POINT('',(0.0866025403784439,-0.64,0.15));
#26742=CARTESIAN_POINT('',(0.0866025403784439,-0.4,0.15));
#26743=CARTESIAN_POINT('',(-0.0866025403784439,-0.64,0.15));
#26744=CARTESIAN_POINT('Origin',(0.173205080756888,-0.4,0.));
#26745=CARTESIAN_POINT('',(0.0866025403784439,-0.4,0.15));
#26746=CARTESIAN_POINT('',(0.0866025403784439,-0.64,0.15));
#26747=CARTESIAN_POINT('Origin',(0.,-0.4,-2.77555756156289E-17));
#26748=CARTESIAN_POINT('Origin',(0.,-0.64,-2.77555756156289E-17));
#26990=UNCERTAINTY_MEASURE_WITH_UNIT(LENGTH_MEASURE(0.001),#27070,
'DISTANCE_ACCURACY_VALUE',
'Maximum model space distance between geometric entities at asserted c
onnectivities');
#26992=UNCERTAINTY_MEASURE_WITH_UNIT(LENGTH_MEASURE(0.001),#27070,
'DISTANCE_ACCURACY_VALUE',
'Maximum model space distance between geometric entities at asserted c
onnectivities');
#27067=(
GEOMETRIC_REPRESENTATION_CONTEXT(3)
GLOBAL_UNCERTAINTY_ASSIGNED_CONTEXT((#26990))
GLOBAL_UNIT_ASSIGNED_CONTEXT((#27070,#27072,#27073))
REPRESENTATION_CONTEXT('','3D')
);
#27069=(
GEOMETRIC_REPRESENTATION_CONTEXT(3)
GLOBAL_UNCERTAINTY_ASSIGNED_CONTEXT((#26992))
GLOBAL_UNIT_ASSIGNED_CONTEXT((#27070,#27072,#27073))
REPRESENTATION_CONTEXT('','3D')
);
#27070=(
LENGTH_UNIT()
NAMED_UNIT(*)
SI_UNIT(.CENTI.,.METRE.)
);
#27072=(
NAMED_UNIT(*)
PLANE_ANGLE_UNIT()
SI_UNIT($,.RADIAN.)
);
#27073=(
NAMED_UNIT(*)
SI_UNIT($,.STERADIAN.)
SOLID_ANGLE_UNIT()
);
#27148=SHAPE_DEFINITION_REPRESENTATION(#27236,#27425);
#27236=PRODUCT_DEFINITION_SHAPE('',$,#27502);
#27425=SHAPE_REPRESENTATION('',(#16278),#27067);
#27427=PRODUCT_DEFINITION_CONTEXT('part definition',#27657,'design');
#27502=PRODUCT_DEFINITION('Cap Screw - M4x16','Cap Screw - M4x16',#27578,
#27427);
#27578=PRODUCT_DEFINITION_FORMATION('',$,#27733);
#27657=APPLICATION_CONTEXT(
'Core Data for Automotive Mechanical Design Process');
#27658=PRODUCT_CONTEXT('part definition',#27657,'mechanical');
#27733=PRODUCT('Cap Screw - M4x16','Cap Screw - M4x16',
'Cap Screw - M4x16',(#27658));
#27798=COLOUR_RGB('Black',0.12,0.14,0.17);
#27799=FILL_AREA_STYLE_COLOUR('',#27798);
#27800=FILL_AREA_STYLE('',(#27799));
#27801=SURFACE_STYLE_FILL_AREA(#27800);
#27802=SURFACE_SIDE_STYLE('',(#27801));
#27803=SURFACE_STYLE_USAGE(.BOTH.,#27802);
#27804=PRESENTATION_STYLE_ASSIGNMENT((#27803));
ENDSEC;
END-ISO-10303-21;
